ISO-10303-21;
HEADER;
/* Generated by software containing ST-Developer
 * from STEP Tools, Inc. (www.steptools.com) 
 */

FILE_DESCRIPTION(
/* description */ ('Two-link friction support arm'),
/* implementation_level */ '2;1');

FILE_NAME(
/* name */ 'Flat Washer - M8.step',
/* time_stamp */ '2026-10-27T20:01:49-07:00',
/* author */ (''),
/* organization */ (''),
/* preprocessor_version */ 'ST-DEVELOPER v20.2',
/* originating_system */ 'Autodesk Translation Framework v15.17.0.0',
/* authorisation */ '');

FILE_SCHEMA (('AUTOMOTIVE_DESIGN { 1 0 10303 214 3 1 1 }'));
ENDSEC;

DATA;
#10=MECHANICAL_DESIGN_GEOMETRIC_PRESENTATION_REPRESENTATION('',(#203),#5492);
#181=SHAPE_REPRESENTATION_RELATIONSHIP('SRR','None',#5575,#192);
#192=ADVANCED_BREP_SHAPE_REPRESENTATION('',(#213),#5489);
#203=STYLED_ITEM('',(#5708),#213);
#213=MANIFOLD_SOLID_BREP('Body1',#3180);
#243=FACE_BOUND('',#700,.T.);
#244=FACE_BOUND('',#702,.T.);
#354=PLANE('',#3514);
#355=PLANE('',#3515);
#503=FACE_OUTER_BOUND('',#697,.T.);
#504=FACE_OUTER_BOUND('',#698,.T.);
#505=FACE_OUTER_BOUND('',#699,.T.);
#506=FACE_OUTER_BOUND('',#701,.T.);
#697=EDGE_LOOP('',(#2792,#2793,#2794,#2795));
#698=EDGE_LOOP('',(#2796,#2797,#2798,#2799));
#699=EDGE_LOOP('',(#2800));
#700=EDGE_LOOP('',(#2801));
#701=EDGE_LOOP('',(#2802));
#702=EDGE_LOOP('',(#2803));
#1012=LINE('',#5230,#1325);
#1013=LINE('',#5236,#1326);
#1325=VECTOR('',#4286,0.42);
#1326=VECTOR('',#4293,0.8);
#1415=CIRCLE('',#3509,0.42);
#1416=CIRCLE('',#3510,0.42);
#1417=CIRCLE('',#3512,0.8);
#1418=CIRCLE('',#3513,0.8);
#1665=VERTEX_POINT('',#5227);
#1666=VERTEX_POINT('',#5229);
#1667=VERTEX_POINT('',#5233);
#1668=VERTEX_POINT('',#5235);
#2050=EDGE_CURVE('',#1665,#1665,#1415,.T.);
#2051=EDGE_CURVE('',#1665,#1666,#1012,.T.);
#2052=EDGE_CURVE('',#1666,#1666,#1416,.T.);
#2053=EDGE_CURVE('',#1667,#1667,#1417,.T.);
#2054=EDGE_CURVE('',#1667,#1668,#1013,.T.);
#2055=EDGE_CURVE('',#1668,#1668,#1418,.T.);
#2792=ORIENTED_EDGE('',*,*,#2050,.F.);
#2793=ORIENTED_EDGE('',*,*,#2051,.T.);
#2794=ORIENTED_EDGE('',*,*,#2052,.T.);
#2795=ORIENTED_EDGE('',*,*,#2051,.F.);
#2796=ORIENTED_EDGE('',*,*,#2053,.F.);
#2797=ORIENTED_EDGE('',*,*,#2054,.T.);
#2798=ORIENTED_EDGE('',*,*,#2055,.T.);
#2799=ORIENTED_EDGE('',*,*,#2054,.F.);
#2800=ORIENTED_EDGE('',*,*,#2053,.T.);
#2801=ORIENTED_EDGE('',*,*,#2050,.T.);
#2802=ORIENTED_EDGE('',*,*,#2055,.F.);
#2803=ORIENTED_EDGE('',*,*,#2052,.F.);
#2988=CYLINDRICAL_SURFACE('',#3508,0.42);
#2989=CYLINDRICAL_SURFACE('',#3511,0.8);
#3134=ADVANCED_FACE('',(#503),#2988,.F.);
#3135=ADVANCED_FACE('',(#504),#2989,.T.);
#3136=ADVANCED_FACE('',(#505,#243),#354,.T.);
#3137=ADVANCED_FACE('',(#506,#244),#355,.F.);
#3180=CLOSED_SHELL('',(#3134,#3135,#3136,#3137));
#3507=AXIS2_PLACEMENT_3D('',#5225,#4280,#4281);
#3508=AXIS2_PLACEMENT_3D('',#5226,#4282,#4283);
#3509=AXIS2_PLACEMENT_3D('',#5228,#4284,#4285);
#3510=AXIS2_PLACEMENT_3D('',#5231,#4287,#4288);
#3511=AXIS2_PLACEMENT_3D('',#5232,#4289,#4290);
#3512=AXIS2_PLACEMENT_3D('',#5234,#4291,#4292);
#3513=AXIS2_PLACEMENT_3D('',#5237,#4294,#4295);
#3514=AXIS2_PLACEMENT_3D('',#5238,#4296,#4297);
#3515=AXIS2_PLACEMENT_3D('',#5239,#4298,#4299);
#4280=DIRECTION('axis',(0.,0.,1.));
#4281=DIRECTION('refdir',(1.,0.,0.));
#4282=DIRECTION('center_axis',(0.,1.,0.));
#4283=DIRECTION('ref_axis',(1.,0.,0.));
#4284=DIRECTION('center_axis',(0.,-1.,0.));
#4285=DIRECTION('ref_axis',(1.,0.,0.));
#4286=DIRECTION('',(0.,-1.,0.));
#4287=DIRECTION('center_axis',(0.,-1.,0.));
#4288=DIRECTION('ref_axis',(1.,0.,0.));
#4289=DIRECTION('center_axis',(0.,1.,0.));
#4290=DIRECTION('ref_axis',(1.,0.,0.));
#4291=DIRECTION('center_axis',(0.,1.,0.));
#4292=DIRECTION('ref_axis',(1.,0.,0.));
#4293=DIRECTION('',(0.,-1.,0.));
#4294=DIRECTION('center_axis',(0.,1.,0.));
#4295=DIRECTION('ref_axis',(1.,0.,0.));
#4296=DIRECTION('center_axis',(0.,1.,0.));
#4297=DIRECTION('ref_axis',(1.,0.,0.));
#4298=DIRECTION('center_axis',(0.,1.,0.));
#4299=DIRECTION('ref_axis',(1.,0.,0.));
#5225=CARTESIAN_POINT('',(0.,0.,0.));
#5226=CARTESIAN_POINT('Origin',(0.,0.,0.));
#5227=CARTESIAN_POINT('',(-0.42,0.16,5.14351655641888E-17));
#5228=CARTESIAN_POINT('Origin',(0.,0.16,0.));
#5229=CARTESIAN_POINT('',(-0.42,0.,5.14351655641888E-17));
#5230=CARTESIAN_POINT('',(-0.42,0.,5.14351655641888E-17));
#5231=CARTESIAN_POINT('Origin',(0.,0.,0.));
#5232=CARTESIAN_POINT('Origin',(0.,0.,0.));
#5233=CARTESIAN_POINT('',(-0.8,0.16,9.79717439317883E-17));
#5234=CARTESIAN_POINT('Origin',(0.,0.16,0.));
#5235=CARTESIAN_POINT('',(-0.8,0.,9.79717439317883E-17));
#5236=CARTESIAN_POINT('',(-0.8,0.,9.79717439317883E-17));
#5237=CARTESIAN_POINT('Origin',(0.,0.,0.));
#5238=CARTESIAN_POINT('Origin',(0.,0.16,0.));
#5239=CARTESIAN_POINT('Origin',(0.,0.,0.));
#5472=UNCERTAINTY_MEASURE_WITH_UNIT(LENGTH_MEASURE(0.001),#5493,
'DISTANCE_ACCURACY_VALUE',
'Maximum model space distance between geometric entities at asserted c
onnectivities');
#5475=UNCERTAINTY_MEASURE_WITH_UNIT(LENGTH_MEASURE(0.001),#5493,
'DISTANCE_ACCURACY_VALUE',
'Maximum model space distance between geometric entities at asserted c
onnectivities');
#5489=(
GEOMETRIC_REPRESENTATION_CONTEXT(3)
GLOBAL_UNCERTAINTY_ASSIGNED_CONTEXT((#5472))
GLOBAL_UNIT_ASSIGNED_CONTEXT((#5493,#5495,#5496))
REPRESENTATION_CONTEXT('','3D')
);
#5492=(
GEOMETRIC_REPRESENTATION_CONTEXT(3)
GLOBAL_UNCERTAINTY_ASSIGNED_CONTEXT((#5475))
GLOBAL_UNIT_ASSIGNED_CONTEXT((#5493,#5495,#5496))
REPRESENTATION_CONTEXT('','3D')
);
#5493=(
LENGTH_UNIT()
NAMED_UNIT(*)
SI_UNIT(.CENTI.,.METRE.)
);
#5495=(
NAMED_UNIT(*)
PLANE_ANGLE_UNIT()
SI_UNIT($,.RADIAN.)
);
#5496=(
NAMED_UNIT(*)
SI_UNIT($,.STERADIAN.)
SOLID_ANGLE_UNIT()
);
#5510=SHAPE_DEFINITION_REPRESENTATION(#5535,#5575);
#5535=PRODUCT_DEFINITION_SHAPE('',$,#5592);
#5575=SHAPE_REPRESENTATION('',(#3507),#5489);
#5578=PRODUCT_DEFINITION_CONTEXT('part definition',#5628,'design');
#5592=PRODUCT_DEFINITION('Flat Washer - M8','Flat Washer - M8',#5608,#5578);
#5608=PRODUCT_DEFINITION_FORMATION('',$,#5643);
#5628=APPLICATION_CONTEXT(
'Core Data for Automotive Mechanical Design Process');
#5629=PRODUCT_CONTEXT('part definition',#5628,'mechanical');
#5643=PRODUCT('Flat Washer - M8','Flat Washer - M8','Flat Washer - M8',
(#5629));
#5702=COLOUR_RGB('Black',0.12,0.14,0.17);
#5703=FILL_AREA_STYLE_COLOUR('',#5702);
#5704=FILL_AREA_STYLE('',(#5703));
#5705=SURFACE_STYLE_FILL_AREA(#5704);
#5706=SURFACE_SIDE_STYLE('',(#5705));
#5707=SURFACE_STYLE_USAGE(.BOTH.,#5706);
#5708=PRESENTATION_STYLE_ASSIGNMENT((#5707));
ENDSEC;
END-ISO-10303-21;
